ISO-10303-21;
HEADER;
/* Generated by software containing ST-Developer
 * from STEP Tools, Inc. (www.steptools.com) 
 */

FILE_DESCRIPTION(
/* description */ ('Double-row support with tensioned shaft'),
/* implementation_level */ '2;1');

FILE_NAME(
/* name */ 'Flange hole reducer (1).step',
/* time_stamp */ '2026-10-27T10:50:35-07:00',
/* author */ (''),
/* organization */ (''),
/* preprocessor_version */ 'ST-DEVELOPER v20.2',
/* originating_system */ 'Autodesk Translation Framework v15.17.0.0',
/* authorisation */ '');

FILE_SCHEMA (('AUTOMOTIVE_DESIGN { 1 0 10303 214 3 1 1 }'));
ENDSEC;

DATA;
#10=MECHANICAL_DESIGN_GEOMETRIC_PRESENTATION_REPRESENTATION('',(#486),#11559);
#422=SHAPE_REPRESENTATION_RELATIONSHIP('SRR','None',#11730,#454);
#454=ADVANCED_BREP_SHAPE_REPRESENTATION('',(#519),#11532);
#486=STYLED_ITEM('',(#11981),#519);
#519=MANIFOLD_SOLID_BREP('Body1',#6331);
#582=FACE_BOUND('',#1365,.T.);
#583=FACE_BOUND('',#1367,.T.);
#719=PLANE('',#6832);
#720=PLANE('',#6833);
#978=FACE_OUTER_BOUND('',#1362,.T.);
#979=FACE_OUTER_BOUND('',#1363,.T.);
#980=FACE_OUTER_BOUND('',#1364,.T.);
#981=FACE_OUTER_BOUND('',#1366,.T.);
#1362=EDGE_LOOP('',(#4612,#4613,#4614,#4615));
#1363=EDGE_LOOP('',(#4616,#4617,#4618,#4619));
#1364=EDGE_LOOP('',(#4620));
#1365=EDGE_LOOP('',(#4621));
#1366=EDGE_LOOP('',(#4622));
#1367=EDGE_LOOP('',(#4623));
#1841=LINE('',#9544,#2388);
#1842=LINE('',#9550,#2389);
#2388=VECTOR('',#7700,0.425);
#2389=VECTOR('',#7707,0.595);
#2878=CIRCLE('',#6827,0.425);
#2879=CIRCLE('',#6828,0.425);
#2880=CIRCLE('',#6830,0.595);
#2881=CIRCLE('',#6831,0.595);
#3121=VERTEX_POINT('',#9541);
#3122=VERTEX_POINT('',#9543);
#3123=VERTEX_POINT('',#9547);
#3124=VERTEX_POINT('',#9549);
#3691=EDGE_CURVE('',#3121,#3121,#2878,.T.);
#3692=EDGE_CURVE('',#3121,#3122,#1841,.T.);
#3693=EDGE_CURVE('',#3122,#3122,#2879,.T.);
#3694=EDGE_CURVE('',#3123,#3123,#2880,.T.);
#3695=EDGE_CURVE('',#3123,#3124,#1842,.T.);
#3696=EDGE_CURVE('',#3124,#3124,#2881,.T.);
#4612=ORIENTED_EDGE('',*,*,#3691,.F.);
#4613=ORIENTED_EDGE('',*,*,#3692,.T.);
#4614=ORIENTED_EDGE('',*,*,#3693,.T.);
#4615=ORIENTED_EDGE('',*,*,#3692,.F.);
#4616=ORIENTED_EDGE('',*,*,#3694,.F.);
#4617=ORIENTED_EDGE('',*,*,#3695,.T.);
#4618=ORIENTED_EDGE('',*,*,#3696,.T.);
#4619=ORIENTED_EDGE('',*,*,#3695,.F.);
#4620=ORIENTED_EDGE('',*,*,#3694,.T.);
#4621=ORIENTED_EDGE('',*,*,#3691,.T.);
#4622=ORIENTED_EDGE('',*,*,#3696,.F.);
#4623=ORIENTED_EDGE('',*,*,#3693,.F.);
#5911=CYLINDRICAL_SURFACE('',#6826,0.425);
#5912=CYLINDRICAL_SURFACE('',#6829,0.595);
#6041=ADVANCED_FACE('',(#978),#5911,.F.);
#6042=ADVANCED_FACE('',(#979),#5912,.T.);
#6043=ADVANCED_FACE('',(#980,#582),#719,.T.);
#6044=ADVANCED_FACE('',(#981,#583),#720,.F.);
#6331=CLOSED_SHELL('',(#6041,#6042,#6043,#6044));
#6825=AXIS2_PLACEMENT_3D('',#9539,#7694,#7695);
#6826=AXIS2_PLACEMENT_3D('',#9540,#7696,#7697);
#6827=AXIS2_PLACEMENT_3D('',#9542,#7698,#7699);
#6828=AXIS2_PLACEMENT_3D('',#9545,#7701,#7702);
#6829=AXIS2_PLACEMENT_3D('',#9546,#7703,#7704);
#6830=AXIS2_PLACEMENT_3D('',#9548,#7705,#7706);
#6831=AXIS2_PLACEMENT_3D('',#9551,#7708,#7709);
#6832=AXIS2_PLACEMENT_3D('',#9552,#7710,#7711);
#6833=AXIS2_PLACEMENT_3D('',#9553,#7712,#7713);
#7694=DIRECTION('axis',(0.,0.,1.));
#7695=DIRECTION('refdir',(1.,0.,0.));
#7696=DIRECTION('center_axis',(0.,1.,0.));
#7697=DIRECTION('ref_axis',(1.,0.,0.));
#7698=DIRECTION('center_axis',(0.,-1.,0.));
#7699=DIRECTION('ref_axis',(1.,0.,0.));
#7700=DIRECTION('',(0.,-1.,0.));
#7701=DIRECTION('center_axis',(0.,-1.,0.));
#7702=DIRECTION('ref_axis',(1.,0.,0.));
#7703=DIRECTION('center_axis',(0.,1.,0.));
#7704=DIRECTION('ref_axis',(1.,0.,0.));
#7705=DIRECTION('center_axis',(0.,1.,0.));
#7706=DIRECTION('ref_axis',(1.,0.,0.));
#7707=DIRECTION('',(0.,-1.,0.));
#7708=DIRECTION('center_axis',(0.,1.,0.));
#7709=DIRECTION('ref_axis',(1.,0.,0.));
#7710=DIRECTION('center_axis',(0.,1.,0.));
#7711=DIRECTION('ref_axis',(1.,0.,0.));
#7712=DIRECTION('center_axis',(0.,1.,0.));
#7713=DIRECTION('ref_axis',(1.,0.,0.));
#9539=CARTESIAN_POINT('',(0.,0.,0.));
#9540=CARTESIAN_POINT('Origin',(-3.2,-0.5,13.2));
#9541=CARTESIAN_POINT('',(-3.625,0.5,13.2));
#9542=CARTESIAN_POINT('Origin',(-3.2,0.5,13.2));
#9543=CARTESIAN_POINT('',(-3.625,-0.5,13.2));
#9544=CARTESIAN_POINT('',(-3.625,-0.5,13.2));
#9545=CARTESIAN_POINT('Origin',(-3.2,-0.5,13.2));
#9546=CARTESIAN_POINT('Origin',(-3.2,-0.5,13.2));
#9547=CARTESIAN_POINT('',(-3.795,0.5,13.2));
#9548=CARTESIAN_POINT('Origin',(-3.2,0.5,13.2));
#9549=CARTESIAN_POINT('',(-3.795,-0.5,13.2));
#9550=CARTESIAN_POINT('',(-3.795,-0.5,13.2));
#9551=CARTESIAN_POINT('Origin',(-3.2,-0.5,13.2));
#9552=CARTESIAN_POINT('Origin',(-3.2,0.5,13.2));
#9553=CARTESIAN_POINT('Origin',(-3.2,-0.5,13.2));
#11495=UNCERTAINTY_MEASURE_WITH_UNIT(LENGTH_MEASURE(0.001),#11560,
'DISTANCE_ACCURACY_VALUE',
'Maximum model space distance between geometric entities at asserted c
onnectivities');
#11522=UNCERTAINTY_MEASURE_WITH_UNIT(LENGTH_MEASURE(0.001),#11560,
'DISTANCE_ACCURACY_VALUE',
'Maximum model space distance between geometric entities at asserted c
onnectivities');
#11532=(
GEOMETRIC_REPRESENTATION_CONTEXT(3)
GLOBAL_UNCERTAINTY_ASSIGNED_CONTEXT((#11495))
GLOBAL_UNIT_ASSIGNED_CONTEXT((#11560,#11562,#11563))
REPRESENTATION_CONTEXT('','3D')
);
#11559=(
GEOMETRIC_REPRESENTATION_CONTEXT(3)
GLOBAL_UNCERTAINTY_ASSIGNED_CONTEXT((#11522))
GLOBAL_UNIT_ASSIGNED_CONTEXT((#11560,#11562,#11563))
REPRESENTATION_CONTEXT('','3D')
);
#11560=(
LENGTH_UNIT()
NAMED_UNIT(*)
SI_UNIT(.CENTI.,.METRE.)
);
#11562=(
NAMED_UNIT(*)
PLANE_ANGLE_UNIT()
SI_UNIT($,.RADIAN.)
);
#11563=(
NAMED_UNIT(*)
SI_UNIT($,.STERADIAN.)
SOLID_ANGLE_UNIT()
);
#11573=SHAPE_DEFINITION_REPRESENTATION(#11609,#11730);
#11609=PRODUCT_DEFINITION_SHAPE('',$,#11767);
#11730=SHAPE_REPRESENTATION('',(#6825),#11532);
#11757=PRODUCT_DEFINITION_CONTEXT('part definition',#11867,'design');
#11767=PRODUCT_DEFINITION('Flange hole reducer (1)',
'Flange hole reducer (1)',#11803,#11757);
#11803=PRODUCT_DEFINITION_FORMATION('',$,#11878);
#11867=APPLICATION_CONTEXT(
'Core Data for Automotive Mechanical Design Process');
#11868=PRODUCT_CONTEXT('part definition',#11867,'mechanical');
#11878=PRODUCT('Flange hole reducer (1)','Flange hole reducer (1)',
'Flange hole reducer (1)',(#11868));
#11975=COLOUR_RGB('Off White',0.89,0.88,0.83);
#11976=FILL_AREA_STYLE_COLOUR('',#11975);
#11977=FILL_AREA_STYLE('',(#11976));
#11978=SURFACE_STYLE_FILL_AREA(#11977);
#11979=SURFACE_SIDE_STYLE('',(#11978));
#11980=SURFACE_STYLE_USAGE(.BOTH.,#11979);
#11981=PRESENTATION_STYLE_ASSIGNMENT((#11980));
ENDSEC;
END-ISO-10303-21;
